ISO-10303-21;
HEADER;
/* Generated by software containing ST-Developer
 * from STEP Tools, Inc. (www.steptools.com) 
 */

FILE_DESCRIPTION(
/* description */ (''),
/* implementation_level */ '2;1');

FILE_NAME(
/* name */ '17_ISO_8734_Dowel_Pin_3x18.step',
/* time_stamp */ '2026-10-21T01:56:51-07:00',
/* author */ (''),
/* organization */ (''),
/* preprocessor_version */ 'ST-DEVELOPER v20.2',
/* originating_system */ 'Autodesk Translation Framework v15.15.0.0',
/* authorisation */ '');

FILE_SCHEMA (('AUTOMOTIVE_DESIGN { 1 0 10303 214 3 1 1 }'));
ENDSEC;

DATA;
#10=MECHANICAL_DESIGN_GEOMETRIC_PRESENTATION_REPRESENTATION('',(#282),#82384);
#244=SHAPE_REPRESENTATION_RELATIONSHIP('SRR','None',#82478,#263);
#263=ADVANCED_BREP_SHAPE_REPRESENTATION('',(#301),#82377);
#282=STYLED_ITEM('',(#82631),#301);
#301=MANIFOLD_SOLID_BREP('Body1',#30673);
#665=CYLINDRICAL_SURFACE('',#32449,1.5);
#1631=CIRCLE('',#32446,1.2);
#1632=CIRCLE('',#32448,1.5);
#1633=CIRCLE('',#32450,1.5);
#1634=CIRCLE('',#32452,1.2);
#2042=CONICAL_SURFACE('',#32447,1.35,0.785398163397448);
#2043=CONICAL_SURFACE('',#32451,1.35,0.785398163397448);
#4639=FACE_OUTER_BOUND('',#6637,.T.);
#4640=FACE_OUTER_BOUND('',#6638,.T.);
#4641=FACE_OUTER_BOUND('',#6639,.T.);
#4642=FACE_OUTER_BOUND('',#6640,.T.);
#4643=FACE_OUTER_BOUND('',#6641,.T.);
#6637=EDGE_LOOP('',(#24331));
#6638=EDGE_LOOP('',(#24332,#24333,#24334,#24335));
#6639=EDGE_LOOP('',(#24336,#24337,#24338,#24339));
#6640=EDGE_LOOP('',(#24340,#24341,#24342,#24343));
#6641=EDGE_LOOP('',(#24344));
#8842=LINE('',#55987,#11148);
#8843=LINE('',#55991,#11149);
#8844=LINE('',#55995,#11150);
#11148=VECTOR('',#37991,1.35);
#11149=VECTOR('',#37996,1.5);
#11150=VECTOR('',#38001,1.35);
#13609=VERTEX_POINT('',#55982);
#13610=VERTEX_POINT('',#55985);
#13611=VERTEX_POINT('',#55989);
#13612=VERTEX_POINT('',#55993);
#17387=EDGE_CURVE('',#13609,#13609,#1631,.T.);
#17388=EDGE_CURVE('',#13610,#13610,#1632,.T.);
#17389=EDGE_CURVE('',#13610,#13609,#8842,.T.);
#17390=EDGE_CURVE('',#13611,#13611,#1633,.T.);
#17391=EDGE_CURVE('',#13611,#13610,#8843,.T.);
#17392=EDGE_CURVE('',#13612,#13612,#1634,.T.);
#17393=EDGE_CURVE('',#13612,#13611,#8844,.T.);
#24331=ORIENTED_EDGE('',*,*,#17387,.F.);
#24332=ORIENTED_EDGE('',*,*,#17388,.F.);
#24333=ORIENTED_EDGE('',*,*,#17389,.T.);
#24334=ORIENTED_EDGE('',*,*,#17387,.T.);
#24335=ORIENTED_EDGE('',*,*,#17389,.F.);
#24336=ORIENTED_EDGE('',*,*,#17390,.F.);
#24337=ORIENTED_EDGE('',*,*,#17391,.T.);
#24338=ORIENTED_EDGE('',*,*,#17388,.T.);
#24339=ORIENTED_EDGE('',*,*,#17391,.F.);
#24340=ORIENTED_EDGE('',*,*,#17392,.F.);
#24341=ORIENTED_EDGE('',*,*,#17393,.T.);
#24342=ORIENTED_EDGE('',*,*,#17390,.T.);
#24343=ORIENTED_EDGE('',*,*,#17393,.F.);
#24344=ORIENTED_EDGE('',*,*,#17392,.T.);
#28634=PLANE('',#32445);
#28635=PLANE('',#32453);
#29967=ADVANCED_FACE('',(#4639),#28634,.T.);
#29968=ADVANCED_FACE('',(#4640),#2042,.T.);
#29969=ADVANCED_FACE('',(#4641),#665,.T.);
#29970=ADVANCED_FACE('',(#4642),#2043,.T.);
#29971=ADVANCED_FACE('',(#4643),#28635,.T.);
#30673=CLOSED_SHELL('',(#29967,#29968,#29969,#29970,#29971));
#32444=AXIS2_PLACEMENT_3D('',#55980,#37981,#37982);
#32445=AXIS2_PLACEMENT_3D('',#55981,#37983,#37984);
#32446=AXIS2_PLACEMENT_3D('',#55983,#37985,#37986);
#32447=AXIS2_PLACEMENT_3D('',#55984,#37987,#37988);
#32448=AXIS2_PLACEMENT_3D('',#55986,#37989,#37990);
#32449=AXIS2_PLACEMENT_3D('',#55988,#37992,#37993);
#32450=AXIS2_PLACEMENT_3D('',#55990,#37994,#37995);
#32451=AXIS2_PLACEMENT_3D('',#55992,#37997,#37998);
#32452=AXIS2_PLACEMENT_3D('',#55994,#37999,#38000);
#32453=AXIS2_PLACEMENT_3D('',#55996,#38002,#38003);
#37981=DIRECTION('axis',(0.,0.,1.));
#37982=DIRECTION('refdir',(1.,0.,0.));
#37983=DIRECTION('center_axis',(-1.,0.,0.));
#37984=DIRECTION('ref_axis',(0.,0.,1.));
#37985=DIRECTION('center_axis',(1.,0.,0.));
#37986=DIRECTION('ref_axis',(0.,0.,-1.));
#37987=DIRECTION('center_axis',(1.,0.,0.));
#37988=DIRECTION('ref_axis',(0.,1.,0.));
#37989=DIRECTION('center_axis',(1.,0.,0.));
#37990=DIRECTION('ref_axis',(0.,0.,-1.));
#37991=DIRECTION('',(-0.707106781186547,0.707106781186548,8.65956056235493E-17));
#37992=DIRECTION('center_axis',(1.,0.,0.));
#37993=DIRECTION('ref_axis',(0.,1.,0.));
#37994=DIRECTION('center_axis',(1.,0.,0.));
#37995=DIRECTION('ref_axis',(0.,0.,-1.));
#37996=DIRECTION('',(-1.,0.,0.));
#37997=DIRECTION('center_axis',(-1.,0.,0.));
#37998=DIRECTION('ref_axis',(0.,1.,0.));
#37999=DIRECTION('center_axis',(1.,0.,0.));
#38000=DIRECTION('ref_axis',(0.,0.,-1.));
#38001=DIRECTION('',(-0.707106781186548,-0.707106781186547,-8.65956056235493E-17));
#38002=DIRECTION('center_axis',(1.,0.,0.));
#38003=DIRECTION('ref_axis',(0.,0.,-1.));
#55980=CARTESIAN_POINT('',(0.,0.,0.));
#55981=CARTESIAN_POINT('Origin',(0.,1.2,0.));
#55982=CARTESIAN_POINT('',(-5.72458747072346E-16,-1.2,-1.46957615897682E-16));
#55983=CARTESIAN_POINT('Origin',(0.,0.,0.));
#55984=CARTESIAN_POINT('Origin',(0.149999999999999,0.,0.));
#55985=CARTESIAN_POINT('',(0.3,-1.5,-1.83697019872103E-16));
#55986=CARTESIAN_POINT('Origin',(0.3,0.,0.));
#55987=CARTESIAN_POINT('',(0.149999999999999,-1.35,-1.65327317884893E-16));
#55988=CARTESIAN_POINT('Origin',(9.,0.,0.));
#55989=CARTESIAN_POINT('',(17.7,-1.5,-1.83697019872103E-16));
#55990=CARTESIAN_POINT('Origin',(17.7,0.,0.));
#55991=CARTESIAN_POINT('',(9.,-1.5,-1.83697019872103E-16));
#55992=CARTESIAN_POINT('Origin',(17.85,0.,0.));
#55993=CARTESIAN_POINT('',(18.,-1.2,-1.46957615897682E-16));
#55994=CARTESIAN_POINT('Origin',(18.,0.,0.));
#55995=CARTESIAN_POINT('',(17.85,-1.35,-1.65327317884893E-16));
#55996=CARTESIAN_POINT('Origin',(18.,0.,0.));
#82356=UNCERTAINTY_MEASURE_WITH_UNIT(LENGTH_MEASURE(0.01),#82385,
'DISTANCE_ACCURACY_VALUE',
'Maximum model space distance between geometric entities at asserted c
onnectivities');
#82363=UNCERTAINTY_MEASURE_WITH_UNIT(LENGTH_MEASURE(0.01),#82385,
'DISTANCE_ACCURACY_VALUE',
'Maximum model space distance between geometric entities at asserted c
onnectivities');
#82377=(
GEOMETRIC_REPRESENTATION_CONTEXT(3)
GLOBAL_UNCERTAINTY_ASSIGNED_CONTEXT((#82356))
GLOBAL_UNIT_ASSIGNED_CONTEXT((#82385,#82387,#82388))
REPRESENTATION_CONTEXT('','3D')
);
#82384=(
GEOMETRIC_REPRESENTATION_CONTEXT(3)
GLOBAL_UNCERTAINTY_ASSIGNED_CONTEXT((#82363))
GLOBAL_UNIT_ASSIGNED_CONTEXT((#82385,#82387,#82388))
REPRESENTATION_CONTEXT('','3D')
);
#82385=(
LENGTH_UNIT()
NAMED_UNIT(*)
SI_UNIT(.MILLI.,.METRE.)
);
#82387=(
NAMED_UNIT(*)
PLANE_ANGLE_UNIT()
SI_UNIT($,.RADIAN.)
);
#82388=(
NAMED_UNIT(*)
SI_UNIT($,.STERADIAN.)
SOLID_ANGLE_UNIT()
);
#82402=SHAPE_DEFINITION_REPRESENTATION(#82422,#82478);
#82422=PRODUCT_DEFINITION_SHAPE('',$,#82499);
#82478=SHAPE_REPRESENTATION('',(#32444),#82377);
#82485=PRODUCT_DEFINITION_CONTEXT('part definition',#82547,'design');
#82499=PRODUCT_DEFINITION('2026-10-20-12-38-37-321',
'17_ISO_8734_Dowel_Pin_3x18',#82519,#82485);
#82519=PRODUCT_DEFINITION_FORMATION('',$,#82562);
#82547=APPLICATION_CONTEXT(
'Core Data for Automotive Mechanical Design Process');
#82548=PRODUCT_CONTEXT('part definition',#82547,'mechanical');
#82562=PRODUCT('2026-10-20-12-38-37-321','17_ISO_8734_Dowel_Pin_3x18',$,
(#82548));
#82625=COLOUR_RGB('Grey',0.48,0.52,0.57);
#82626=FILL_AREA_STYLE_COLOUR('',#82625);
#82627=FILL_AREA_STYLE('',(#82626));
#82628=SURFACE_STYLE_FILL_AREA(#82627);
#82629=SURFACE_SIDE_STYLE('',(#82628));
#82630=SURFACE_STYLE_USAGE(.BOTH.,#82629);
#82631=PRESENTATION_STYLE_ASSIGNMENT((#82630));
ENDSEC;
END-ISO-10303-21;
